ISO-10303-21;
HEADER;
/* Generated by software containing ST-Developer
 * from STEP Tools, Inc. (www.steptools.com) 
 */

FILE_DESCRIPTION(
/* description */ ('STEP AP214'),
/* implementation_level */ '2;1');

FILE_NAME(
/* name */ 'Washer.step',
/* time_stamp */ '2026-11-15T14:55:55-08:00',
/* author */ (''),
/* organization */ (''),
/* preprocessor_version */ 'ST-DEVELOPER v20.2',
/* originating_system */ 'Autodesk Translation Framework v15.17.0.0',
/* authorisation */ '');

FILE_SCHEMA (('AUTOMOTIVE_DESIGN { 1 0 10303 214 3 1 1 }'));
ENDSEC;

DATA;
#10=MECHANICAL_DESIGN_GEOMETRIC_PRESENTATION_REPRESENTATION('',(#935),#57079);
#875=SHAPE_REPRESENTATION_RELATIONSHIP('SRR','None',#57261,#904);
#904=ADVANCED_BREP_SHAPE_REPRESENTATION('',(#972),#57053);
#935=STYLED_ITEM('',(#57444),#972);
#972=MANIFOLD_SOLID_BREP('Body1',#24535);
#1089=FACE_BOUND('',#3875,.T.);
#1090=FACE_BOUND('',#3876,.T.);
#1091=FACE_BOUND('',#3878,.T.);
#1092=FACE_BOUND('',#3879,.T.);
#1492=PLANE('',#25350);
#1493=PLANE('',#25355);
#1494=PLANE('',#25360);
#1495=PLANE('',#25362);
#1496=PLANE('',#25365);
#1497=PLANE('',#25367);
#1498=PLANE('',#25368);
#1499=PLANE('',#25369);
#2406=FACE_OUTER_BOUND('',#3870,.T.);
#2407=FACE_OUTER_BOUND('',#3871,.T.);
#2408=FACE_OUTER_BOUND('',#3872,.T.);
#2409=FACE_OUTER_BOUND('',#3873,.T.);
#2410=FACE_OUTER_BOUND('',#3874,.T.);
#2411=FACE_OUTER_BOUND('',#3877,.T.);
#2412=FACE_OUTER_BOUND('',#3880,.T.);
#2413=FACE_OUTER_BOUND('',#3881,.T.);
#2414=FACE_OUTER_BOUND('',#3882,.T.);
#2415=FACE_OUTER_BOUND('',#3883,.T.);
#2416=FACE_OUTER_BOUND('',#3884,.T.);
#2417=FACE_OUTER_BOUND('',#3885,.T.);
#2418=FACE_OUTER_BOUND('',#3886,.T.);
#2419=FACE_OUTER_BOUND('',#3887,.T.);
#2420=FACE_OUTER_BOUND('',#3888,.T.);
#2421=FACE_OUTER_BOUND('',#3889,.T.);
#3870=EDGE_LOOP('',(#17012,#17013,#17014,#17015));
#3871=EDGE_LOOP('',(#17016,#17017,#17018,#17019));
#3872=EDGE_LOOP('',(#17020,#17021,#17022,#17023));
#3873=EDGE_LOOP('',(#17024,#17025,#17026,#17027));
#3874=EDGE_LOOP('',(#17028,#17029,#17030,#17031,#17032,#17033,#17034,#17035,
#17036,#17037,#17038,#17039));
#3875=EDGE_LOOP('',(#17040));
#3876=EDGE_LOOP('',(#17041));
#3877=EDGE_LOOP('',(#17042,#17043,#17044,#17045,#17046,#17047,#17048,#17049,
#17050,#17051,#17052,#17053));
#3878=EDGE_LOOP('',(#17054));
#3879=EDGE_LOOP('',(#17055));
#3880=EDGE_LOOP('',(#17056,#17057,#17058,#17059));
#3881=EDGE_LOOP('',(#17060,#17061,#17062,#17063));
#3882=EDGE_LOOP('',(#17064,#17065,#17066,#17067));
#3883=EDGE_LOOP('',(#17068,#17069,#17070,#17071));
#3884=EDGE_LOOP('',(#17072,#17073,#17074,#17075));
#3885=EDGE_LOOP('',(#17076,#17077,#17078,#17079));
#3886=EDGE_LOOP('',(#17080,#17081,#17082,#17083));
#3887=EDGE_LOOP('',(#17084,#17085,#17086,#17087));
#3888=EDGE_LOOP('',(#17088,#17089,#17090,#17091));
#3889=EDGE_LOOP('',(#17092,#17093,#17094,#17095));
#5595=LINE('',#36033,#7562);
#5596=LINE('',#36039,#7563);
#5597=LINE('',#36046,#7564);
#5598=LINE('',#36049,#7565);
#5599=LINE('',#36055,#7566);
#5600=LINE('',#36058,#7567);
#5601=LINE('',#36062,#7568);
#5602=LINE('',#36066,#7569);
#5603=LINE('',#36071,#7570);
#5604=LINE('',#36075,#7571);
#5605=LINE('',#36076,#7572);
#5606=LINE('',#36077,#7573);
#5607=LINE('',#36081,#7574);
#5608=LINE('',#36082,#7575);
#5609=LINE('',#36084,#7576);
#5610=LINE('',#36086,#7577);
#5611=LINE('',#36090,#7578);
#5612=LINE('',#36095,#7579);
#5613=LINE('',#36098,#7580);
#5614=LINE('',#36099,#7581);
#5615=LINE('',#36101,#7582);
#5616=LINE('',#36103,#7583);
#5617=LINE('',#36106,#7584);
#5618=LINE('',#36108,#7585);
#5619=LINE('',#36110,#7586);
#5620=LINE('',#36112,#7587);
#7562=VECTOR('',#28735,0.6);
#7563=VECTOR('',#28742,0.6);
#7564=VECTOR('',#28749,1000.);
#7565=VECTOR('',#28752,1000.);
#7566=VECTOR('',#28757,1000.);
#7567=VECTOR('',#28760,1000.);
#7568=VECTOR('',#28763,1000.);
#7569=VECTOR('',#28766,1000.);
#7570=VECTOR('',#28771,1000.);
#7571=VECTOR('',#28774,1000.);
#7572=VECTOR('',#28775,1000.);
#7573=VECTOR('',#28776,1000.);
#7574=VECTOR('',#28779,1000.);
#7575=VECTOR('',#28780,1000.);
#7576=VECTOR('',#28781,1000.);
#7577=VECTOR('',#28782,1000.);
#7578=VECTOR('',#28785,1000.);
#7579=VECTOR('',#28790,1000.);
#7580=VECTOR('',#28795,1000.);
#7581=VECTOR('',#28796,1000.);
#7582=VECTOR('',#28799,1000.);
#7583=VECTOR('',#28802,1000.);
#7584=VECTOR('',#28807,1000.);
#7585=VECTOR('',#28810,1000.);
#7586=VECTOR('',#28813,1000.);
#7587=VECTOR('',#28816,1000.);
#9374=CIRCLE('',#25339,0.6);
#9375=CIRCLE('',#25340,0.6);
#9376=CIRCLE('',#25342,0.6);
#9377=CIRCLE('',#25343,0.6);
#9378=CIRCLE('',#25345,4.8);
#9379=CIRCLE('',#25346,4.8);
#9380=CIRCLE('',#25348,6.15);
#9381=CIRCLE('',#25349,6.15);
#9382=CIRCLE('',#25351,1.6);
#9383=CIRCLE('',#25352,1.6);
#9384=CIRCLE('',#25353,1.6);
#9385=CIRCLE('',#25354,1.6);
#9386=CIRCLE('',#25356,1.6);
#9387=CIRCLE('',#25357,1.6);
#9388=CIRCLE('',#25358,1.6);
#9389=CIRCLE('',#25359,1.6);
#10635=VERTEX_POINT('',#36030);
#10636=VERTEX_POINT('',#36032);
#10637=VERTEX_POINT('',#36036);
#10638=VERTEX_POINT('',#36038);
#10639=VERTEX_POINT('',#36042);
#10640=VERTEX_POINT('',#36043);
#10641=VERTEX_POINT('',#36045);
#10642=VERTEX_POINT('',#36047);
#10643=VERTEX_POINT('',#36051);
#10644=VERTEX_POINT('',#36052);
#10645=VERTEX_POINT('',#36054);
#10646=VERTEX_POINT('',#36056);
#10647=VERTEX_POINT('',#36060);
#10648=VERTEX_POINT('',#36061);
#10649=VERTEX_POINT('',#36063);
#10650=VERTEX_POINT('',#36065);
#10651=VERTEX_POINT('',#36068);
#10652=VERTEX_POINT('',#36070);
#10653=VERTEX_POINT('',#36072);
#10654=VERTEX_POINT('',#36074);
#10655=VERTEX_POINT('',#36079);
#10656=VERTEX_POINT('',#36080);
#10657=VERTEX_POINT('',#36083);
#10658=VERTEX_POINT('',#36085);
#10659=VERTEX_POINT('',#36087);
#10660=VERTEX_POINT('',#36089);
#10661=VERTEX_POINT('',#36092);
#10662=VERTEX_POINT('',#36094);
#13051=EDGE_CURVE('',#10635,#10635,#9374,.T.);
#13052=EDGE_CURVE('',#10635,#10636,#5595,.T.);
#13053=EDGE_CURVE('',#10636,#10636,#9375,.T.);
#13054=EDGE_CURVE('',#10637,#10637,#9376,.T.);
#13055=EDGE_CURVE('',#10637,#10638,#5596,.T.);
#13056=EDGE_CURVE('',#10638,#10638,#9377,.T.);
#13057=EDGE_CURVE('',#10639,#10640,#9378,.T.);
#13058=EDGE_CURVE('',#10639,#10641,#5597,.T.);
#13059=EDGE_CURVE('',#10641,#10642,#9379,.T.);
#13060=EDGE_CURVE('',#10640,#10642,#5598,.T.);
#13061=EDGE_CURVE('',#10643,#10644,#9380,.T.);
#13062=EDGE_CURVE('',#10643,#10645,#5599,.T.);
#13063=EDGE_CURVE('',#10645,#10646,#9381,.T.);
#13064=EDGE_CURVE('',#10644,#10646,#5600,.T.);
#13065=EDGE_CURVE('',#10647,#10648,#5601,.T.);
#13066=EDGE_CURVE('',#10648,#10649,#9382,.T.);
#13067=EDGE_CURVE('',#10649,#10650,#5602,.T.);
#13068=EDGE_CURVE('',#10650,#10643,#9383,.T.);
#13069=EDGE_CURVE('',#10644,#10651,#9384,.T.);
#13070=EDGE_CURVE('',#10651,#10652,#5603,.T.);
#13071=EDGE_CURVE('',#10652,#10653,#9385,.T.);
#13072=EDGE_CURVE('',#10653,#10654,#5604,.T.);
#13073=EDGE_CURVE('',#10654,#10639,#5605,.T.);
#13074=EDGE_CURVE('',#10640,#10647,#5606,.T.);
#13075=EDGE_CURVE('',#10655,#10656,#5607,.T.);
#13076=EDGE_CURVE('',#10642,#10655,#5608,.T.);
#13077=EDGE_CURVE('',#10657,#10641,#5609,.T.);
#13078=EDGE_CURVE('',#10658,#10657,#5610,.T.);
#13079=EDGE_CURVE('',#10659,#10658,#9386,.T.);
#13080=EDGE_CURVE('',#10660,#10659,#5611,.T.);
#13081=EDGE_CURVE('',#10646,#10660,#9387,.T.);
#13082=EDGE_CURVE('',#10661,#10645,#9388,.T.);
#13083=EDGE_CURVE('',#10662,#10661,#5612,.T.);
#13084=EDGE_CURVE('',#10656,#10662,#9389,.T.);
#13085=EDGE_CURVE('',#10648,#10656,#5613,.T.);
#13086=EDGE_CURVE('',#10647,#10655,#5614,.T.);
#13087=EDGE_CURVE('',#10649,#10662,#5615,.T.);
#13088=EDGE_CURVE('',#10650,#10661,#5616,.T.);
#13089=EDGE_CURVE('',#10651,#10660,#5617,.T.);
#13090=EDGE_CURVE('',#10652,#10659,#5618,.T.);
#13091=EDGE_CURVE('',#10653,#10658,#5619,.T.);
#13092=EDGE_CURVE('',#10654,#10657,#5620,.T.);
#17012=ORIENTED_EDGE('',*,*,#13051,.T.);
#17013=ORIENTED_EDGE('',*,*,#13052,.T.);
#17014=ORIENTED_EDGE('',*,*,#13053,.F.);
#17015=ORIENTED_EDGE('',*,*,#13052,.F.);
#17016=ORIENTED_EDGE('',*,*,#13054,.T.);
#17017=ORIENTED_EDGE('',*,*,#13055,.T.);
#17018=ORIENTED_EDGE('',*,*,#13056,.F.);
#17019=ORIENTED_EDGE('',*,*,#13055,.F.);
#17020=ORIENTED_EDGE('',*,*,#13057,.F.);
#17021=ORIENTED_EDGE('',*,*,#13058,.T.);
#17022=ORIENTED_EDGE('',*,*,#13059,.T.);
#17023=ORIENTED_EDGE('',*,*,#13060,.F.);
#17024=ORIENTED_EDGE('',*,*,#13061,.F.);
#17025=ORIENTED_EDGE('',*,*,#13062,.T.);
#17026=ORIENTED_EDGE('',*,*,#13063,.T.);
#17027=ORIENTED_EDGE('',*,*,#13064,.F.);
#17028=ORIENTED_EDGE('',*,*,#13065,.T.);
#17029=ORIENTED_EDGE('',*,*,#13066,.T.);
#17030=ORIENTED_EDGE('',*,*,#13067,.T.);
#17031=ORIENTED_EDGE('',*,*,#13068,.T.);
#17032=ORIENTED_EDGE('',*,*,#13061,.T.);
#17033=ORIENTED_EDGE('',*,*,#13069,.T.);
#17034=ORIENTED_EDGE('',*,*,#13070,.T.);
#17035=ORIENTED_EDGE('',*,*,#13071,.T.);
#17036=ORIENTED_EDGE('',*,*,#13072,.T.);
#17037=ORIENTED_EDGE('',*,*,#13073,.T.);
#17038=ORIENTED_EDGE('',*,*,#13057,.T.);
#17039=ORIENTED_EDGE('',*,*,#13074,.T.);
#17040=ORIENTED_EDGE('',*,*,#13051,.F.);
#17041=ORIENTED_EDGE('',*,*,#13054,.F.);
#17042=ORIENTED_EDGE('',*,*,#13075,.F.);
#17043=ORIENTED_EDGE('',*,*,#13076,.F.);
#17044=ORIENTED_EDGE('',*,*,#13059,.F.);
#17045=ORIENTED_EDGE('',*,*,#13077,.F.);
#17046=ORIENTED_EDGE('',*,*,#13078,.F.);
#17047=ORIENTED_EDGE('',*,*,#13079,.F.);
#17048=ORIENTED_EDGE('',*,*,#13080,.F.);
#17049=ORIENTED_EDGE('',*,*,#13081,.F.);
#17050=ORIENTED_EDGE('',*,*,#13063,.F.);
#17051=ORIENTED_EDGE('',*,*,#13082,.F.);
#17052=ORIENTED_EDGE('',*,*,#13083,.F.);
#17053=ORIENTED_EDGE('',*,*,#13084,.F.);
#17054=ORIENTED_EDGE('',*,*,#13056,.T.);
#17055=ORIENTED_EDGE('',*,*,#13053,.T.);
#17056=ORIENTED_EDGE('',*,*,#13075,.T.);
#17057=ORIENTED_EDGE('',*,*,#13085,.F.);
#17058=ORIENTED_EDGE('',*,*,#13065,.F.);
#17059=ORIENTED_EDGE('',*,*,#13086,.T.);
#17060=ORIENTED_EDGE('',*,*,#13084,.T.);
#17061=ORIENTED_EDGE('',*,*,#13087,.F.);
#17062=ORIENTED_EDGE('',*,*,#13066,.F.);
#17063=ORIENTED_EDGE('',*,*,#13085,.T.);
#17064=ORIENTED_EDGE('',*,*,#13083,.T.);
#17065=ORIENTED_EDGE('',*,*,#13088,.F.);
#17066=ORIENTED_EDGE('',*,*,#13067,.F.);
#17067=ORIENTED_EDGE('',*,*,#13087,.T.);
#17068=ORIENTED_EDGE('',*,*,#13082,.T.);
#17069=ORIENTED_EDGE('',*,*,#13062,.F.);
#17070=ORIENTED_EDGE('',*,*,#13068,.F.);
#17071=ORIENTED_EDGE('',*,*,#13088,.T.);
#17072=ORIENTED_EDGE('',*,*,#13081,.T.);
#17073=ORIENTED_EDGE('',*,*,#13089,.F.);
#17074=ORIENTED_EDGE('',*,*,#13069,.F.);
#17075=ORIENTED_EDGE('',*,*,#13064,.T.);
#17076=ORIENTED_EDGE('',*,*,#13080,.T.);
#17077=ORIENTED_EDGE('',*,*,#13090,.F.);
#17078=ORIENTED_EDGE('',*,*,#13070,.F.);
#17079=ORIENTED_EDGE('',*,*,#13089,.T.);
#17080=ORIENTED_EDGE('',*,*,#13079,.T.);
#17081=ORIENTED_EDGE('',*,*,#13091,.F.);
#17082=ORIENTED_EDGE('',*,*,#13071,.F.);
#17083=ORIENTED_EDGE('',*,*,#13090,.T.);
#17084=ORIENTED_EDGE('',*,*,#13078,.T.);
#17085=ORIENTED_EDGE('',*,*,#13092,.F.);
#17086=ORIENTED_EDGE('',*,*,#13072,.F.);
#17087=ORIENTED_EDGE('',*,*,#13091,.T.);
#17088=ORIENTED_EDGE('',*,*,#13077,.T.);
#17089=ORIENTED_EDGE('',*,*,#13058,.F.);
#17090=ORIENTED_EDGE('',*,*,#13073,.F.);
#17091=ORIENTED_EDGE('',*,*,#13092,.T.);
#17092=ORIENTED_EDGE('',*,*,#13076,.T.);
#17093=ORIENTED_EDGE('',*,*,#13086,.F.);
#17094=ORIENTED_EDGE('',*,*,#13074,.F.);
#17095=ORIENTED_EDGE('',*,*,#13060,.T.);
#22810=CYLINDRICAL_SURFACE('',#25338,0.6);
#22811=CYLINDRICAL_SURFACE('',#25341,0.6);
#22812=CYLINDRICAL_SURFACE('',#25344,4.8);
#22813=CYLINDRICAL_SURFACE('',#25347,6.15);
#22814=CYLINDRICAL_SURFACE('',#25361,1.6);
#22815=CYLINDRICAL_SURFACE('',#25363,1.6);
#22816=CYLINDRICAL_SURFACE('',#25364,1.6);
#22817=CYLINDRICAL_SURFACE('',#25366,1.6);
#23398=ADVANCED_FACE('',(#2406),#22810,.F.);
#23399=ADVANCED_FACE('',(#2407),#22811,.F.);
#23400=ADVANCED_FACE('',(#2408),#22812,.F.);
#23401=ADVANCED_FACE('',(#2409),#22813,.T.);
#23402=ADVANCED_FACE('',(#2410,#1089,#1090),#1492,.T.);
#23403=ADVANCED_FACE('',(#2411,#1091,#1092),#1493,.F.);
#23404=ADVANCED_FACE('',(#2412),#1494,.F.);
#23405=ADVANCED_FACE('',(#2413),#22814,.T.);
#23406=ADVANCED_FACE('',(#2414),#1495,.F.);
#23407=ADVANCED_FACE('',(#2415),#22815,.F.);
#23408=ADVANCED_FACE('',(#2416),#22816,.F.);
#23409=ADVANCED_FACE('',(#2417),#1496,.F.);
#23410=ADVANCED_FACE('',(#2418),#22817,.T.);
#23411=ADVANCED_FACE('',(#2419),#1497,.F.);
#23412=ADVANCED_FACE('',(#2420),#1498,.F.);
#23413=ADVANCED_FACE('',(#2421),#1499,.F.);
#24535=CLOSED_SHELL('',(#23398,#23399,#23400,#23401,#23402,#23403,#23404,
#23405,#23406,#23407,#23408,#23409,#23410,#23411,#23412,#23413));
#25337=AXIS2_PLACEMENT_3D('',#36028,#28729,#28730);
#25338=AXIS2_PLACEMENT_3D('',#36029,#28731,#28732);
#25339=AXIS2_PLACEMENT_3D('',#36031,#28733,#28734);
#25340=AXIS2_PLACEMENT_3D('',#36034,#28736,#28737);
#25341=AXIS2_PLACEMENT_3D('',#36035,#28738,#28739);
#25342=AXIS2_PLACEMENT_3D('',#36037,#28740,#28741);
#25343=AXIS2_PLACEMENT_3D('',#36040,#28743,#28744);
#25344=AXIS2_PLACEMENT_3D('',#36041,#28745,#28746);
#25345=AXIS2_PLACEMENT_3D('',#36044,#28747,#28748);
#25346=AXIS2_PLACEMENT_3D('',#36048,#28750,#28751);
#25347=AXIS2_PLACEMENT_3D('',#36050,#28753,#28754);
#25348=AXIS2_PLACEMENT_3D('',#36053,#28755,#28756);
#25349=AXIS2_PLACEMENT_3D('',#36057,#28758,#28759);
#25350=AXIS2_PLACEMENT_3D('',#36059,#28761,#28762);
#25351=AXIS2_PLACEMENT_3D('',#36064,#28764,#28765);
#25352=AXIS2_PLACEMENT_3D('',#36067,#28767,#28768);
#25353=AXIS2_PLACEMENT_3D('',#36069,#28769,#28770);
#25354=AXIS2_PLACEMENT_3D('',#36073,#28772,#28773);
#25355=AXIS2_PLACEMENT_3D('',#36078,#28777,#28778);
#25356=AXIS2_PLACEMENT_3D('',#36088,#28783,#28784);
#25357=AXIS2_PLACEMENT_3D('',#36091,#28786,#28787);
#25358=AXIS2_PLACEMENT_3D('',#36093,#28788,#28789);
#25359=AXIS2_PLACEMENT_3D('',#36096,#28791,#28792);
#25360=AXIS2_PLACEMENT_3D('',#36097,#28793,#28794);
#25361=AXIS2_PLACEMENT_3D('',#36100,#28797,#28798);
#25362=AXIS2_PLACEMENT_3D('',#36102,#28800,#28801);
#25363=AXIS2_PLACEMENT_3D('',#36104,#28803,#28804);
#25364=AXIS2_PLACEMENT_3D('',#36105,#28805,#28806);
#25365=AXIS2_PLACEMENT_3D('',#36107,#28808,#28809);
#25366=AXIS2_PLACEMENT_3D('',#36109,#28811,#28812);
#25367=AXIS2_PLACEMENT_3D('',#36111,#28814,#28815);
#25368=AXIS2_PLACEMENT_3D('',#36113,#28817,#28818);
#25369=AXIS2_PLACEMENT_3D('',#36114,#28819,#28820);
#28729=DIRECTION('axis',(0.,0.,1.));
#28730=DIRECTION('refdir',(1.,0.,0.));
#28731=DIRECTION('center_axis',(-1.,0.,0.));
#28732=DIRECTION('ref_axis',(0.,0.,1.));
#28733=DIRECTION('center_axis',(1.,0.,0.));
#28734=DIRECTION('ref_axis',(0.,0.,-1.));
#28735=DIRECTION('',(-1.,0.,0.));
#28736=DIRECTION('center_axis',(1.,0.,0.));
#28737=DIRECTION('ref_axis',(0.,0.,-1.));
#28738=DIRECTION('center_axis',(-1.,0.,0.));
#28739=DIRECTION('ref_axis',(0.,0.,1.));
#28740=DIRECTION('center_axis',(1.,0.,0.));
#28741=DIRECTION('ref_axis',(0.,0.,-1.));
#28742=DIRECTION('',(-1.,0.,0.));
#28743=DIRECTION('center_axis',(1.,0.,0.));
#28744=DIRECTION('ref_axis',(0.,0.,-1.));
#28745=DIRECTION('center_axis',(-1.,0.,0.));
#28746=DIRECTION('ref_axis',(0.,1.,6.12323399573676E-17));
#28747=DIRECTION('center_axis',(-1.,0.,0.));
#28748=DIRECTION('ref_axis',(0.,0.,-1.));
#28749=DIRECTION('',(-1.,0.,0.));
#28750=DIRECTION('center_axis',(-1.,0.,0.));
#28751=DIRECTION('ref_axis',(0.,0.,-1.));
#28752=DIRECTION('',(-1.,0.,0.));
#28753=DIRECTION('center_axis',(-1.,0.,0.));
#28754=DIRECTION('ref_axis',(0.,1.,6.12323399573677E-17));
#28755=DIRECTION('center_axis',(1.,0.,0.));
#28756=DIRECTION('ref_axis',(0.,0.,-1.));
#28757=DIRECTION('',(-1.,0.,0.));
#28758=DIRECTION('center_axis',(1.,0.,0.));
#28759=DIRECTION('ref_axis',(0.,0.,-1.));
#28760=DIRECTION('',(-1.,0.,0.));
#28761=DIRECTION('center_axis',(1.,0.,0.));
#28762=DIRECTION('ref_axis',(0.,0.,-1.));
#28763=DIRECTION('',(0.,1.020425574104E-15,-1.));
#28764=DIRECTION('center_axis',(1.,0.,0.));
#28765=DIRECTION('ref_axis',(0.,0.,-1.));
#28766=DIRECTION('',(0.,1.,0.));
#28767=DIRECTION('center_axis',(-1.,0.,0.));
#28768=DIRECTION('ref_axis',(0.,0.,-1.));
#28769=DIRECTION('center_axis',(-1.,0.,0.));
#28770=DIRECTION('ref_axis',(0.,0.,-1.));
#28771=DIRECTION('',(0.,-1.,0.));
#28772=DIRECTION('center_axis',(1.,0.,0.));
#28773=DIRECTION('ref_axis',(0.,0.,-1.));
#28774=DIRECTION('',(0.,-1.020425574104E-15,-1.));
#28775=DIRECTION('',(0.,1.,-1.61730259095139E-16));
#28776=DIRECTION('',(0.,-1.,-1.61730259095139E-16));
#28777=DIRECTION('center_axis',(1.,0.,0.));
#28778=DIRECTION('ref_axis',(0.,0.,-1.));
#28779=DIRECTION('',(0.,1.020425574104E-15,-1.));
#28780=DIRECTION('',(0.,-1.,-1.61730259095139E-16));
#28781=DIRECTION('',(0.,1.,-1.61730259095139E-16));
#28782=DIRECTION('',(0.,-1.020425574104E-15,-1.));
#28783=DIRECTION('center_axis',(1.,0.,0.));
#28784=DIRECTION('ref_axis',(0.,0.,-1.));
#28785=DIRECTION('',(0.,-1.,0.));
#28786=DIRECTION('center_axis',(-1.,0.,0.));
#28787=DIRECTION('ref_axis',(0.,0.,-1.));
#28788=DIRECTION('center_axis',(-1.,0.,0.));
#28789=DIRECTION('ref_axis',(0.,0.,-1.));
#28790=DIRECTION('',(0.,1.,0.));
#28791=DIRECTION('center_axis',(1.,0.,0.));
#28792=DIRECTION('ref_axis',(0.,0.,-1.));
#28793=DIRECTION('center_axis',(0.,1.,1.020425574104E-15));
#28794=DIRECTION('ref_axis',(0.,-1.020425574104E-15,1.));
#28795=DIRECTION('',(-1.,0.,0.));
#28796=DIRECTION('',(-1.,0.,0.));
#28797=DIRECTION('center_axis',(-1.,0.,0.));
#28798=DIRECTION('ref_axis',(0.,0.,1.));
#28799=DIRECTION('',(-1.,0.,0.));
#28800=DIRECTION('center_axis',(0.,0.,1.));
#28801=DIRECTION('ref_axis',(1.,0.,0.));
#28802=DIRECTION('',(-1.,0.,0.));
#28803=DIRECTION('center_axis',(-1.,0.,0.));
#28804=DIRECTION('ref_axis',(0.,0.,1.));
#28805=DIRECTION('center_axis',(-1.,0.,0.));
#28806=DIRECTION('ref_axis',(0.,0.,1.));
#28807=DIRECTION('',(-1.,0.,0.));
#28808=DIRECTION('center_axis',(0.,0.,-1.));
#28809=DIRECTION('ref_axis',(-1.,0.,0.));
#28810=DIRECTION('',(-1.,0.,0.));
#28811=DIRECTION('center_axis',(-1.,0.,0.));
#28812=DIRECTION('ref_axis',(0.,0.,1.));
#28813=DIRECTION('',(-1.,0.,0.));
#28814=DIRECTION('center_axis',(0.,1.,-1.020425574104E-15));
#28815=DIRECTION('ref_axis',(0.,1.020425574104E-15,1.));
#28816=DIRECTION('',(-1.,0.,0.));
#28817=DIRECTION('center_axis',(0.,1.61730259095139E-16,1.));
#28818=DIRECTION('ref_axis',(0.,-1.,1.61730259095139E-16));
#28819=DIRECTION('center_axis',(0.,1.61730259095139E-16,-1.));
#28820=DIRECTION('ref_axis',(0.,1.,1.61730259095139E-16));
#36028=CARTESIAN_POINT('',(0.,0.,0.));
#36029=CARTESIAN_POINT('Origin',(1.,-6.65,2.1));
#36030=CARTESIAN_POINT('',(1.,-6.65,1.5));
#36031=CARTESIAN_POINT('Origin',(1.,-6.65,2.1));
#36032=CARTESIAN_POINT('',(0.,-6.65,1.5));
#36033=CARTESIAN_POINT('',(1.,-6.65,1.5));
#36034=CARTESIAN_POINT('Origin',(0.,-6.65,2.1));
#36035=CARTESIAN_POINT('Origin',(1.,-6.65,-2.1));
#36036=CARTESIAN_POINT('',(1.,-6.65,-2.7));
#36037=CARTESIAN_POINT('Origin',(1.,-6.65,-2.1));
#36038=CARTESIAN_POINT('',(0.,-6.65,-2.7));
#36039=CARTESIAN_POINT('',(1.,-6.65,-2.7));
#36040=CARTESIAN_POINT('Origin',(0.,-6.65,-2.1));
#36041=CARTESIAN_POINT('Origin',(1.,-0.45,0.));
#36042=CARTESIAN_POINT('',(1.,-5.23330429724056,0.400000000000003));
#36043=CARTESIAN_POINT('',(1.,-5.23330429724056,-0.4));
#36044=CARTESIAN_POINT('Origin',(1.,-0.45,0.));
#36045=CARTESIAN_POINT('',(0.,-5.23330429724056,0.400000000000003));
#36046=CARTESIAN_POINT('',(1.,-5.23330429724056,0.400000000000003));
#36047=CARTESIAN_POINT('',(0.,-5.23330429724056,-0.4));
#36048=CARTESIAN_POINT('Origin',(0.,-0.45,0.));
#36049=CARTESIAN_POINT('',(1.,-5.23330429724056,-0.4));
#36050=CARTESIAN_POINT('Origin',(1.,2.60208521396521E-15,2.71050543121376E-16));
#36051=CARTESIAN_POINT('',(1.,-4.48705828929949,-4.2058064516129));
#36052=CARTESIAN_POINT('',(1.,-4.48705828929949,4.2058064516129));
#36053=CARTESIAN_POINT('Origin',(1.,2.60208521396521E-15,2.71050543121376E-16));
#36054=CARTESIAN_POINT('',(0.,-4.48705828929949,-4.2058064516129));
#36055=CARTESIAN_POINT('',(1.,-4.48705828929949,-4.2058064516129));
#36056=CARTESIAN_POINT('',(0.,-4.48705828929949,4.2058064516129));
#36057=CARTESIAN_POINT('Origin',(0.,2.60208521396521E-15,2.71050543121376E-16));
#36058=CARTESIAN_POINT('',(1.,-4.48705828929949,4.2058064516129));
#36059=CARTESIAN_POINT('Origin',(1.,-0.45,0.));
#36060=CARTESIAN_POINT('',(1.,-8.25,-0.4));
#36061=CARTESIAN_POINT('',(1.,-8.25,-2.1));
#36062=CARTESIAN_POINT('',(1.,-8.25,-2.1));
#36063=CARTESIAN_POINT('',(1.,-6.65,-3.7));
#36064=CARTESIAN_POINT('Origin',(1.,-6.65,-2.1));
#36065=CARTESIAN_POINT('',(1.,-5.65442304749123,-3.7));
#36066=CARTESIAN_POINT('',(1.,-5.65442304749123,-3.7));
#36067=CARTESIAN_POINT('Origin',(1.,-5.65442304749123,-5.3));
#36068=CARTESIAN_POINT('',(1.,-5.65442304749123,3.7));
#36069=CARTESIAN_POINT('Origin',(1.,-5.65442304749123,5.3));
#36070=CARTESIAN_POINT('',(1.,-6.65,3.7));
#36071=CARTESIAN_POINT('',(1.,-5.65442304749123,3.7));
#36072=CARTESIAN_POINT('',(1.,-8.25,2.1));
#36073=CARTESIAN_POINT('Origin',(1.,-6.65,2.1));
#36074=CARTESIAN_POINT('',(1.,-8.25,0.4));
#36075=CARTESIAN_POINT('',(1.,-8.25,2.1));
#36076=CARTESIAN_POINT('',(1.,-5.23330429724056,0.4));
#36077=CARTESIAN_POINT('',(1.,-5.23330429724056,-0.4));
#36078=CARTESIAN_POINT('Origin',(0.,-0.45,0.));
#36079=CARTESIAN_POINT('',(0.,-8.25,-0.4));
#36080=CARTESIAN_POINT('',(0.,-8.25,-2.1));
#36081=CARTESIAN_POINT('',(0.,-8.25,-2.1));
#36082=CARTESIAN_POINT('',(0.,-5.23330429724056,-0.4));
#36083=CARTESIAN_POINT('',(0.,-8.25,0.4));
#36084=CARTESIAN_POINT('',(0.,-5.23330429724056,0.4));
#36085=CARTESIAN_POINT('',(0.,-8.25,2.1));
#36086=CARTESIAN_POINT('',(0.,-8.25,2.1));
#36087=CARTESIAN_POINT('',(0.,-6.65,3.7));
#36088=CARTESIAN_POINT('Origin',(0.,-6.65,2.1));
#36089=CARTESIAN_POINT('',(0.,-5.65442304749123,3.7));
#36090=CARTESIAN_POINT('',(0.,-5.65442304749123,3.7));
#36091=CARTESIAN_POINT('Origin',(0.,-5.65442304749123,5.3));
#36092=CARTESIAN_POINT('',(0.,-5.65442304749123,-3.7));
#36093=CARTESIAN_POINT('Origin',(0.,-5.65442304749123,-5.3));
#36094=CARTESIAN_POINT('',(0.,-6.65,-3.7));
#36095=CARTESIAN_POINT('',(0.,-5.65442304749123,-3.7));
#36096=CARTESIAN_POINT('Origin',(0.,-6.65,-2.1));
#36097=CARTESIAN_POINT('Origin',(1.,-8.25,-2.1));
#36098=CARTESIAN_POINT('',(1.,-8.25,-2.1));
#36099=CARTESIAN_POINT('',(1.,-8.25,-0.4));
#36100=CARTESIAN_POINT('Origin',(1.,-6.65,-2.1));
#36101=CARTESIAN_POINT('',(1.,-6.65,-3.7));
#36102=CARTESIAN_POINT('Origin',(1.,-5.65442304749123,-3.7));
#36103=CARTESIAN_POINT('',(1.,-5.65442304749123,-3.7));
#36104=CARTESIAN_POINT('Origin',(1.,-5.65442304749123,-5.3));
#36105=CARTESIAN_POINT('Origin',(1.,-5.65442304749123,5.3));
#36106=CARTESIAN_POINT('',(1.,-5.65442304749123,3.7));
#36107=CARTESIAN_POINT('Origin',(1.,-5.65442304749123,3.7));
#36108=CARTESIAN_POINT('',(1.,-6.65,3.7));
#36109=CARTESIAN_POINT('Origin',(1.,-6.65,2.1));
#36110=CARTESIAN_POINT('',(1.,-8.25,2.1));
#36111=CARTESIAN_POINT('Origin',(1.,-8.25,2.1));
#36112=CARTESIAN_POINT('',(1.,-8.25,0.4));
#36113=CARTESIAN_POINT('Origin',(1.,-5.23330429724056,0.4));
#36114=CARTESIAN_POINT('Origin',(1.,-5.23330429724056,-0.4));
#57014=UNCERTAINTY_MEASURE_WITH_UNIT(LENGTH_MEASURE(0.01),#57080,
'DISTANCE_ACCURACY_VALUE',
'Maximum model space distance between geometric entities at asserted c
onnectivities');
#57040=UNCERTAINTY_MEASURE_WITH_UNIT(LENGTH_MEASURE(0.01),#57080,
'DISTANCE_ACCURACY_VALUE',
'Maximum model space distance between geometric entities at asserted c
onnectivities');
#57053=(
GEOMETRIC_REPRESENTATION_CONTEXT(3)
GLOBAL_UNCERTAINTY_ASSIGNED_CONTEXT((#57014))
GLOBAL_UNIT_ASSIGNED_CONTEXT((#57080,#57082,#57083))
REPRESENTATION_CONTEXT('','3D')
);
#57079=(
GEOMETRIC_REPRESENTATION_CONTEXT(3)
GLOBAL_UNCERTAINTY_ASSIGNED_CONTEXT((#57040))
GLOBAL_UNIT_ASSIGNED_CONTEXT((#57080,#57082,#57083))
REPRESENTATION_CONTEXT('','3D')
);
#57080=(
LENGTH_UNIT()
NAMED_UNIT(*)
SI_UNIT(.MILLI.,.METRE.)
);
#57082=(
NAMED_UNIT(*)
PLANE_ANGLE_UNIT()
SI_UNIT($,.RADIAN.)
);
#57083=(
NAMED_UNIT(*)
SI_UNIT($,.STERADIAN.)
SOLID_ANGLE_UNIT()
);
#57096=SHAPE_DEFINITION_REPRESENTATION(#57140,#57261);
#57140=PRODUCT_DEFINITION_SHAPE('',$,#57300);
#57261=SHAPE_REPRESENTATION('',(#25337),#57053);
#57287=PRODUCT_DEFINITION_CONTEXT('part definition',#57403,'design');
#57300=PRODUCT_DEFINITION('Washer','Washer',#57338,#57287);
#57338=PRODUCT_DEFINITION_FORMATION('',$,#57417);
#57403=APPLICATION_CONTEXT(
'Core Data for Automotive Mechanical Design Process');
#57404=PRODUCT_CONTEXT('part definition',#57403,'mechanical');
#57417=PRODUCT('Washer','Washer',$,(#57404));
#57444=PRESENTATION_STYLE_ASSIGNMENT((#57446));
#57446=SURFACE_STYLE_USAGE(.BOTH.,#57448);
#57448=SURFACE_SIDE_STYLE('',(#57450));
#57450=SURFACE_STYLE_FILL_AREA(#57452);
#57452=FILL_AREA_STYLE('Opaque(202,209,238)',(#57454));
#57454=FILL_AREA_STYLE_COLOUR('Opaque(202,209,238)',#57456);
#57456=COLOUR_RGB('Opaque(202,209,238)',0.792156862745098,0.819607843137255,
0.933333333333333);
ENDSEC;
END-ISO-10303-21;
